ISO-10303-21;
HEADER;
FILE_DESCRIPTION (('STEP AP214'),
    '1' );
FILE_NAME ('socket head cap screw_iso_ISO 4762 M4 x 12 - 12N.step',
    '2026-10-08T07:58:12',
    ( '' ),
    ( '' ),
    'SwSTEP 2.0',
    'SolidWorks 2026',
    '' );
FILE_SCHEMA (( 'AUTOMOTIVE_DESIGN' ));
ENDSEC;

DATA;
#10=ORIENTED_EDGE ( 'NONE', *, *, #1282, .F. ) ;
#72=DIRECTION ( 'NONE',  ( -1.000000000000000000, -0.000000000000000000, -0.000000000000000000 ) ) ;
#118=AXIS2_PLACEMENT_3D ( 'NONE', #27781, #9730, #4445 ) ;
#133=( LENGTH_UNIT ( ) NAMED_UNIT ( * ) SI_UNIT ( .MILLI., .METRE. ) );
#321=CARTESIAN_POINT ( 'NONE',  ( 0.000000000000000000, 0.000000000000000000, 3.299999999999999822 ) ) ;
#322=DIRECTION ( 'NONE',  ( 0.000000000000000000, -0.5000000000000011102, -0.8660254037844379305 ) ) ;
#391=ORIENTED_EDGE ( 'NONE', *, *, #25603, .F. ) ;
#464=SHAPE_REPRESENTATION_RELATIONSHIP ( 'NONE' , 'NONE' ,  #22175, #21775 ) ;
#504=ORIENTED_EDGE ( 'NONE', *, *, #9364, .F. ) ;
#582=ADVANCED_FACE ( 'NONE', ( #13110, #10068 ), #33561, .T. ) ;
#648=DIRECTION ( 'NONE',  ( 0.000000000000000000, -0.4999999999999990563, 0.8660254037844391517 ) ) ;
#649=ORIENTED_EDGE ( 'NONE', *, *, #18552, .F. ) ;
#653=ORIENTED_EDGE ( 'NONE', *, *, #32062, .T. ) ;
#694=EDGE_LOOP ( 'NONE', ( #19337, #26108, #32446, #26781 ) ) ;
#742=EDGE_LOOP ( 'NONE', ( #22101, #21274, #7659, #32959, #16898 ) ) ;
#751=DIRECTION ( 'NONE',  ( 0.000000000000000000, 0.000000000000000000, 1.000000000000000000 ) ) ;
#784=ADVANCED_FACE ( 'NONE', ( #16487 ), #3096, .F. ) ;
#795=SURFACE_STYLE_FILL_AREA ( #10535 ) ;
#905=EDGE_LOOP ( 'NONE', ( #26424, #10889, #20231, #20681, #20609 ) ) ;
#990=DIRECTION ( 'NONE',  ( -1.000000000000000000, -0.000000000000000000, -0.000000000000000000 ) ) ;
#1012=CARTESIAN_POINT ( 'NONE',  ( 4.000000000000000000, 0.000000000000000000, 0.000000000000000000 ) ) ;
#1033=AXIS2_PLACEMENT_3D ( 'NONE', #1708, #30335, #2058 ) ;
#1070=EDGE_CURVE ( 'NONE', #10890, #31219, #20910, .T. ) ;
#1163=DIRECTION ( 'NONE',  ( 0.000000000000000000, 1.000000000000000000, -1.222984857324291014E-15 ) ) ;
#1279=DIRECTION ( 'NONE',  ( -1.000000000000000000, -0.000000000000000000, -0.000000000000000000 ) ) ;
#1282=EDGE_CURVE ( 'NONE', #22150, #13858, #18398, .T. ) ;
#1292=EDGE_CURVE ( 'NONE', #9623, #30416, #28733, .T. ) ;
#1308=CIRCLE ( 'NONE', #24706, 2.000000000000000888 ) ;
#1381=CARTESIAN_POINT ( 'NONE',  ( 0.1999999999999987899, 0.000000000000000000, 0.000000000000000000 ) ) ;
#1595=PLANE ( 'NONE',  #22922 ) ;
#1631=EDGE_CURVE ( 'NONE', #14984, #23772, #7602, .T. ) ;
#1658=FACE_OUTER_BOUND ( 'NONE', #33344, .T. ) ;
#1673=LINE ( 'NONE', #14117, #24865 ) ;
#1692=EDGE_CURVE ( 'NONE', #30073, #15658, #28705, .T. ) ;
#1708=CARTESIAN_POINT ( 'NONE',  ( 4.000000000000003553, 0.000000000000000000, 0.000000000000000000 ) ) ;
#1885=( GEOMETRIC_REPRESENTATION_CONTEXT ( 3 ) GLOBAL_UNCERTAINTY_ASSIGNED_CONTEXT ( ( #2920 ) ) GLOBAL_UNIT_ASSIGNED_CONTEXT ( ( #133, #15793, #15959 ) ) REPRESENTATION_CONTEXT ( 'NONE', 'WORKASPACE' ) );
#1987=DIRECTION ( 'NONE',  ( 0.000000000000000000, -0.4999999999999990563, 0.8660254037844391517 ) ) ;
#2058=DIRECTION ( 'NONE',  ( 0.000000000000000000, 0.000000000000000000, 1.000000000000000000 ) ) ;
#2182=VERTEX_POINT ( 'NONE', #22836 ) ;
#2230=EDGE_CURVE ( 'NONE', #2182, #32112, #19509, .T. ) ;
#2293=LINE ( 'NONE', #7916, #8862 ) ;
#2311=DIRECTION ( 'NONE',  ( -1.000000000000000000, -0.000000000000000000, -0.000000000000000000 ) ) ;
#2391=VECTOR ( 'NONE', #322, 1000.000000000000114 ) ;
#2399=CARTESIAN_POINT ( 'NONE',  ( 2.000000000000000000, -1.329782007511004727, 0.7677500000000014868 ) ) ;
#2404=AXIS2_PLACEMENT_3D ( 'NONE', #8872, #11941, #4266 ) ;
#2415=DIRECTION ( 'NONE',  ( -0.000000000000000000, 1.100686371591861952E-15, 1.000000000000000000 ) ) ;
#2476=VERTEX_POINT ( 'NONE', #2399 ) ;
#2552=CLOSED_SHELL ( 'NONE', ( #14178, #11432, #7090, #30837, #30292, #9393, #21364, #29876, #20785, #33222, #582, #29313, #784, #22912, #3831, #30402, #13477, #17247, #31221, #21046, #25635, #9358, #22087, #18319, #5590, #32889, #8098 ) ) ;
#2560=DIRECTION ( 'NONE',  ( 0.000000000000000000, 0.000000000000000000, -1.000000000000000000 ) ) ;
#2574=AXIS2_PLACEMENT_3D ( 'NONE', #8335, #13936, #6089 ) ;
#2577=CARTESIAN_POINT ( 'NONE',  ( 4.200000000000001954, 0.000000000000000000, 0.000000000000000000 ) ) ;
#2632=DIRECTION ( 'NONE',  ( 0.000000000000000000, 0.000000000000000000, 1.000000000000000000 ) ) ;
#2673=VECTOR ( 'NONE', #2311, 1000.000000000000000 ) ;
#2700=FILL_AREA_STYLE_COLOUR ( '', #6226 ) ;
#2729=ORIENTED_EDGE ( 'NONE', *, *, #1692, .T. ) ;
#2771=ORIENTED_EDGE ( 'NONE', *, *, #17842, .F. ) ;
#2778=CARTESIAN_POINT ( 'NONE',  ( 2.000000000000000000, 0.000000000000000000, 0.000000000000000000 ) ) ;
#2797=CARTESIAN_POINT ( 'NONE',  ( 0.1999999999999987899, 4.041334437186265510E-16, -3.299999999999999822 ) ) ;
#2798=EDGE_LOOP ( 'NONE', ( #23207, #14517, #8782, #25710 ) ) ;
#2801=DIRECTION ( 'NONE',  ( 0.000000000000000000, 0.4999999999999990008, -0.8660254037844391517 ) ) ;
#2814=CYLINDRICAL_SURFACE ( 'NONE', #13238, 2.000000000000000888 ) ;
#2835=EDGE_LOOP ( 'NONE', ( #7498, #12892, #504 ) ) ;
#2837=ORIENTED_EDGE ( 'NONE', *, *, #12643, .F. ) ;
#2920=UNCERTAINTY_MEASURE_WITH_UNIT (LENGTH_MEASURE( 1.000000000000000082E-05 ), #133, 'distance_accuracy_value', 'NONE');
#2947=CIRCLE ( 'NONE', #10031, 3.299999999999999822 ) ;
#3013=DIRECTION ( 'NONE',  ( 0.000000000000000000, -1.000000000000000000, 0.000000000000000000 ) ) ;
#3096=TOROIDAL_SURFACE ( 'NONE', #2574, 2.200000000000001066, 0.2000000000000000111 ) ;
#3129=LINE ( 'NONE', #21346, #19229 ) ;
#3139=EDGE_CURVE ( 'NONE', #24872, #5170, #30289, .T. ) ;
#3141=FACE_OUTER_BOUND ( 'NONE', #18059, .T. ) ;
#3258=FACE_OUTER_BOUND ( 'NONE', #3573, .T. ) ;
#3339=CARTESIAN_POINT ( 'NONE',  ( 16.00000000000000000, 0.000000000000000000, 0.000000000000000000 ) ) ;
#3402=ORIENTED_EDGE ( 'NONE', *, *, #11389, .T. ) ;
#3467=DIRECTION ( 'NONE',  ( -1.000000000000000000, -0.000000000000000000, -0.000000000000000000 ) ) ;
#3499=ORIENTED_EDGE ( 'NONE', *, *, #3139, .T. ) ;
#3573=EDGE_LOOP ( 'NONE', ( #31224, #24700, #29102 ) ) ;
#3638=VECTOR ( 'NONE', #26653, 1000.000000000000000 ) ;
#3674=DIRECTION ( 'NONE',  ( 0.000000000000000000, 0.000000000000000000, 1.000000000000000000 ) ) ;
#3722=CARTESIAN_POINT ( 'NONE',  ( 2.000000000000000000, 0.8865213383406687075, -1.535500000000000975 ) ) ;
#3739=DIRECTION ( 'NONE',  ( -1.000000000000000000, -0.000000000000000000, -0.000000000000000000 ) ) ;
#3831=ADVANCED_FACE ( 'NONE', ( #4828 ), #1595, .T. ) ;
#3865=CARTESIAN_POINT ( 'NONE',  ( 2.000000000000000000, -0.8865213383406721492, -1.535499999999998977 ) ) ;
#3874=DIRECTION ( 'NONE',  ( 0.000000000000000000, 0.000000000000000000, -1.000000000000000000 ) ) ;
#3959=PRODUCT_DEFINITION_CONTEXT ( 'detailed design', #25297, 'design' ) ;
#4053=CARTESIAN_POINT ( 'NONE',  ( 2.000000000000000000, 0.000000000000000000, 0.000000000000000000 ) ) ;
#4155=VERTEX_POINT ( 'NONE', #15884 ) ;
#4242=ORIENTED_EDGE ( 'NONE', *, *, #5161, .T. ) ;
#4266=DIRECTION ( 'NONE',  ( 1.000000000000000000, 0.000000000000000000, 0.000000000000000000 ) ) ;
#4359=CIRCLE ( 'NONE', #33212, 2.200000000000001066 ) ;
#4386=DIRECTION ( 'NONE',  ( -1.000000000000000000, -0.000000000000000000, -0.000000000000000000 ) ) ;
#4445=DIRECTION ( 'NONE',  ( 0.000000000000000000, 0.000000000000000000, -1.000000000000000000 ) ) ;
#4479=CARTESIAN_POINT ( 'NONE',  ( -31.74999999999995737, 0.000000000000000000, 0.000000000000000000 ) ) ;
#4495=CIRCLE ( 'NONE', #5059, 0.2000000000000000944 ) ;
#4543=CARTESIAN_POINT ( 'NONE',  ( 2.000000000000000000, 1.773042676681340968, -2.276824562219559311E-15 ) ) ;
#4544=TOROIDAL_SURFACE ( 'NONE', #18149, 3.299999999999999822, 0.2000000000000000111 ) ;
#4584=UNCERTAINTY_MEASURE_WITH_UNIT (LENGTH_MEASURE( 1.000000000000000082E-05 ), #13398, 'distance_accuracy_value', 'NONE');
#4599=COLOUR_RGB ( '', 0.08235294, 0.09019608, 0.10196078) ;
#4644=ORIENTED_EDGE ( 'NONE', *, *, #18831, .F. ) ;
#4694=AXIS2_PLACEMENT_3D ( 'NONE', #30527, #5140, #7369 ) ;
#4748=DIRECTION ( 'NONE',  ( 1.000000000000000000, 0.000000000000000000, 0.000000000000000000 ) ) ;
#4756=EDGE_CURVE ( 'NONE', #6483, #25501, #10469, .T. ) ;
#4828=FACE_OUTER_BOUND ( 'NONE', #742, .T. ) ;
#4859=DIRECTION ( 'NONE',  ( 0.000000000000000000, 1.000000000000000000, -1.100686371591861952E-15 ) ) ;
#4881=CARTESIAN_POINT ( 'NONE',  ( 4.000000000000000000, 0.000000000000000000, 0.000000000000000000 ) ) ;
#4921=CARTESIAN_POINT ( 'NONE',  ( 2.000000000000000000, 1.773042676681340968, -2.276824562219559311E-15 ) ) ;
#4935=ORIENTED_EDGE ( 'NONE', *, *, #26240, .F. ) ;
#4954=SHAPE_DEFINITION_REPRESENTATION ( #24647, #22175 ) ;
#5014=DIRECTION ( 'NONE',  ( 0.000000000000000000, -1.000000000000000000, 1.222984857324291014E-15 ) ) ;
#5059=AXIS2_PLACEMENT_3D ( 'NONE', #2797, #23575, #31410 ) ;
#5140=DIRECTION ( 'NONE',  ( -1.000000000000000000, -0.000000000000000000, -0.000000000000000000 ) ) ;
#5152=VERTEX_POINT ( 'NONE', #19238 ) ;
#5161=EDGE_CURVE ( 'NONE', #30416, #25924, #4359, .T. ) ;
#5170=VERTEX_POINT ( 'NONE', #18740 ) ;
#5238=CARTESIAN_POINT ( 'NONE',  ( 4.200000000000001954, 0.000000000000000000, 0.000000000000000000 ) ) ;
#5273=EDGE_LOOP ( 'NONE', ( #649, #29485, #28143, #26822, #653 ) ) ;
#5341=DIRECTION ( 'NONE',  ( 1.000000000000000000, 0.000000000000000000, 0.000000000000000000 ) ) ;
#5357=AXIS2_PLACEMENT_3D ( 'NONE', #16149, #990, #26540 ) ;
#5420=CYLINDRICAL_SURFACE ( 'NONE', #15138, 3.500000000000000000 ) ;
#5533=DIRECTION ( 'NONE',  ( 0.000000000000000000, 0.000000000000000000, -1.000000000000000000 ) ) ;
#5534=CONICAL_SURFACE ( 'NONE', #22955, 1.535500000000000087, 1.047197551196590748 ) ;
#5558=DIRECTION ( 'NONE',  ( 0.000000000000000000, 0.000000000000000000, 1.000000000000000000 ) ) ;
#5590=ADVANCED_FACE ( 'NONE', ( #28368 ), #30422, .F. ) ;
#5654=AXIS2_PLACEMENT_3D ( 'NONE', #16409, #3467, #751 ) ;
#5727=PRESENTATION_STYLE_ASSIGNMENT (( #29243 ) ) ;
#5753=ORIENTED_EDGE ( 'NONE', *, *, #1070, .T. ) ;
#5807=DIRECTION ( 'NONE',  ( 1.000000000000000000, 0.000000000000000000, 0.000000000000000000 ) ) ;
#5808=AXIS2_PLACEMENT_3D ( 'NONE', #30844, #10725, #2560 ) ;
#5848=VERTEX_POINT ( 'NONE', #21521 ) ;
#5852=DIRECTION ( 'NONE',  ( 0.000000000000000000, 0.000000000000000000, -1.000000000000000000 ) ) ;
#5866=DIRECTION ( 'NONE',  ( 0.000000000000000000, 0.000000000000000000, 1.000000000000000000 ) ) ;
#5875=AXIS2_PLACEMENT_3D ( 'NONE', #9804, #33475, #22748 ) ;
#5892=CARTESIAN_POINT ( 'NONE',  ( 2.000000000000000000, 1.329782007511004727, -0.7677500000000019309 ) ) ;
#5982=FACE_OUTER_BOUND ( 'NONE', #23453, .T. ) ;
#6001=ORIENTED_EDGE ( 'NONE', *, *, #12243, .F. ) ;
#6079=ORIENTED_EDGE ( 'NONE', *, *, #26985, .T. ) ;
#6089=DIRECTION ( 'NONE',  ( 0.000000000000000000, 0.000000000000000000, -1.000000000000000000 ) ) ;
#6125=DIRECTION ( 'NONE',  ( 0.000000000000000000, 0.000000000000000000, 1.000000000000000000 ) ) ;
#6133=ORIENTED_EDGE ( 'NONE', *, *, #32062, .F. ) ;
#6151=VECTOR ( 'NONE', #8100, 1000.000000000000000 ) ;
#6185=VERTEX_POINT ( 'NONE', #11307 ) ;
#6226=COLOUR_RGB ( '', 0.08235294, 0.09019608, 0.10196078) ;
#6260=ORIENTED_EDGE ( 'NONE', *, *, #31980, .F. ) ;
#6262=CARTESIAN_POINT ( 'NONE',  ( 2.000000000000000000, -1.877893248421449134E-15, -1.535500000000000087 ) ) ;
#6386=DIRECTION ( 'NONE',  ( 0.000000000000000000, -0.4999999999999990563, 0.8660254037844391517 ) ) ;
#6483=VERTEX_POINT ( 'NONE', #8466 ) ;
#6686=CIRCLE ( 'NONE', #7789, 3.500000000000000000 ) ;
#6725=CIRCLE ( 'NONE', #23584, 3.500000000000000000 ) ;
#6781=ORIENTED_EDGE ( 'NONE', *, *, #17712, .F. ) ;
#6955=CARTESIAN_POINT ( 'NONE',  ( 0.000000000000000000, 1.773042676681340968, -2.276824562219559311E-15 ) ) ;
#6990=DIRECTION ( 'NONE',  ( -1.000000000000000000, -0.000000000000000000, -0.000000000000000000 ) ) ;
#7042=CARTESIAN_POINT ( 'NONE',  ( 2.000000000000000000, -1.773042676681340524, 1.734723475976807094E-15 ) ) ;
#7074=LINE ( 'NONE', #7410, #11594 ) ;
#7090=ADVANCED_FACE ( 'NONE', ( #15761 ), #33126, .F. ) ;
#7193=ORIENTED_EDGE ( 'NONE', *, *, #18831, .T. ) ;
#7196=ORIENTED_EDGE ( 'NONE', *, *, #17216, .T. ) ;
#7205=ORIENTED_EDGE ( 'NONE', *, *, #9276, .F. ) ;
#7258=CIRCLE ( 'NONE', #20849, 2.000000000000000888 ) ;
#7291=EDGE_CURVE ( 'NONE', #15658, #25924, #8654, .T. ) ;
#7369=DIRECTION ( 'NONE',  ( 0.000000000000000000, 0.000000000000000000, 1.000000000000000000 ) ) ;
#7391=DIRECTION ( 'NONE',  ( 0.000000000000000000, -0.8660254037844391517, -0.4999999999999991118 ) ) ;
#7410=CARTESIAN_POINT ( 'NONE',  ( 2.000000000000000000, 1.880445160090761061E-16, -1.535500000000000087 ) ) ;
#7417=CARTESIAN_POINT ( 'NONE',  ( 0.000000000000000000, -0.8865213383406685965, 1.535500000000000531 ) ) ;
#7498=ORIENTED_EDGE ( 'NONE', *, *, #11384, .T. ) ;
#7564=DIRECTION ( 'NONE',  ( -1.000000000000000000, -0.000000000000000000, -0.000000000000000000 ) ) ;
#7586=ORIENTED_EDGE ( 'NONE', *, *, #31980, .T. ) ;
#7602=LINE ( 'NONE', #20532, #16221 ) ;
#7652=FACE_OUTER_BOUND ( 'NONE', #694, .T. ) ;
#7655=DIRECTION ( 'NONE',  ( 0.000000000000000000, 0.000000000000000000, -1.000000000000000000 ) ) ;
#7659=ORIENTED_EDGE ( 'NONE', *, *, #12243, .T. ) ;
#7718=ORIENTED_EDGE ( 'NONE', *, *, #26985, .F. ) ;
#7754=ORIENTED_EDGE ( 'NONE', *, *, #10342, .F. ) ;
#7789=AXIS2_PLACEMENT_3D ( 'NONE', #28682, #5341, #2632 ) ;
#7803=AXIS2_PLACEMENT_3D ( 'NONE', #4921, #4748, #7655 ) ;
#7835=( GEOMETRIC_REPRESENTATION_CONTEXT ( 3 ) GLOBAL_UNCERTAINTY_ASSIGNED_CONTEXT ( ( #4584 ) ) GLOBAL_UNIT_ASSIGNED_CONTEXT ( ( #13398, #31309, #18358 ) ) REPRESENTATION_CONTEXT ( 'NONE', 'WORKASPACE' ) );
#7838=LINE ( 'NONE', #28283, #2391 ) ;
#7899=DIRECTION ( 'NONE',  ( 0.000000000000000000, -0.4999999999999990563, 0.8660254037844391517 ) ) ;
#7916=CARTESIAN_POINT ( 'NONE',  ( 2.000000000000000000, 0.8865213383406687075, -1.535500000000000975 ) ) ;
#7958=PLANE ( 'NONE',  #26289 ) ;
#8084=CARTESIAN_POINT ( 'NONE',  ( 0.000000000000000000, -1.773042676681340524, 1.734723475976807094E-15 ) ) ;
#8098=ADVANCED_FACE ( 'NONE', ( #29854 ), #23906, .F. ) ;
#8100=DIRECTION ( 'NONE',  ( -1.000000000000000000, -0.000000000000000000, -0.000000000000000000 ) ) ;
#8111=DIRECTION ( 'NONE',  ( 1.000000000000000000, 0.000000000000000000, 0.000000000000000000 ) ) ;
#8116=AXIS2_PLACEMENT_3D ( 'NONE', #16259, #23931, #13692 ) ;
#8135=CARTESIAN_POINT ( 'NONE',  ( 15.61000000000001364, 0.000000000000000000, 0.000000000000000000 ) ) ;
#8255=CARTESIAN_POINT ( 'NONE',  ( 16.00000000000000000, 1.610000000000000098, 0.000000000000000000 ) ) ;
#8284=FACE_OUTER_BOUND ( 'NONE', #2835, .T. ) ;
#8298=CARTESIAN_POINT ( 'NONE',  ( 4.200000000000001954, 0.000000000000000000, -2.200000000000001066 ) ) ;
#8335=CARTESIAN_POINT ( 'NONE',  ( 4.200000000000001954, 0.000000000000000000, 0.000000000000000000 ) ) ;
#8352=DIRECTION ( 'NONE',  ( 0.000000000000000000, 0.000000000000000000, -1.000000000000000000 ) ) ;
#8358=CARTESIAN_POINT ( 'NONE',  ( 2.000000000000000000, 0.000000000000000000, 0.000000000000000000 ) ) ;
#8385=CARTESIAN_POINT ( 'NONE',  ( 16.00000000000000000, 0.000000000000000000, 0.000000000000000000 ) ) ;
#8400=VERTEX_POINT ( 'NONE', #15186 ) ;
#8466=CARTESIAN_POINT ( 'NONE',  ( 0.1999999999999987899, 0.000000000000000000, 3.500000000000000000 ) ) ;
#8558=ORIENTED_EDGE ( 'NONE', *, *, #16401, .F. ) ;
#8654=CIRCLE ( 'NONE', #8116, 0.2000000000000000944 ) ;
#8663=ORIENTED_EDGE ( 'NONE', *, *, #15758, .T. ) ;
#8782=ORIENTED_EDGE ( 'NONE', *, *, #1292, .T. ) ;
#8862=VECTOR ( 'NONE', #5014, 1000.000000000000000 ) ;
#8872=CARTESIAN_POINT ( 'NONE',  ( 0.000000000000000000, 0.000000000000000000, 0.000000000000000000 ) ) ;
#8947=ORIENTED_EDGE ( 'NONE', *, *, #12286, .T. ) ;
#9107=CARTESIAN_POINT ( 'NONE',  ( 2.000000000000000000, -1.773042676681340524, 1.734723475976807094E-15 ) ) ;
#9170=DIRECTION ( 'NONE',  ( 0.000000000000000000, 0.000000000000000000, 1.000000000000000000 ) ) ;
#9248=DIRECTION ( 'NONE',  ( 0.000000000000000000, 0.8660254037844380415, -0.5000000000000012212 ) ) ;
#9276=EDGE_CURVE ( 'NONE', #29718, #5152, #21539, .T. ) ;
#9285=ORIENTED_EDGE ( 'NONE', *, *, #18558, .F. ) ;
#9358=ADVANCED_FACE ( 'NONE', ( #3258 ), #11110, .F. ) ;
#9364=EDGE_CURVE ( 'NONE', #5152, #9697, #10733, .T. ) ;
#9393=ADVANCED_FACE ( 'NONE', ( #23877 ), #9625, .T. ) ;
#9454=CARTESIAN_POINT ( 'NONE',  ( 2.000000000000000000, -0.8865213383406685965, 1.535500000000000531 ) ) ;
#9462=ORIENTED_EDGE ( 'NONE', *, *, #22802, .F. ) ;
#9496=FACE_OUTER_BOUND ( 'NONE', #14711, .T. ) ;
#9535=CARTESIAN_POINT ( 'NONE',  ( 0.000000000000000000, 0.8865213383406723713, 1.535499999999998755 ) ) ;
#9562=DIRECTION ( 'NONE',  ( -1.000000000000000000, -0.000000000000000000, -0.000000000000000000 ) ) ;
#9607=AXIS2_PLACEMENT_3D ( 'NONE', #33592, #10274, #6125 ) ;
#9623=VERTEX_POINT ( 'NONE', #27943 ) ;
#9625=CONICAL_SURFACE ( 'NONE', #13440, 1.610000000000000098, 0.7853981633974652654 ) ;
#9635=VECTOR ( 'NONE', #33144, 1000.000000000000000 ) ;
#9684=( NAMED_UNIT ( * ) SI_UNIT ( $, .STERADIAN. ) SOLID_ANGLE_UNIT ( ) );
#9697=VERTEX_POINT ( 'NONE', #29998 ) ;
#9730=DIRECTION ( 'NONE',  ( 0.000000000000000000, -1.000000000000000000, 0.000000000000000000 ) ) ;
#9760=CARTESIAN_POINT ( 'NONE',  ( 0.000000000000000000, 0.000000000000000000, 0.000000000000000000 ) ) ;
#9799=DIRECTION ( 'NONE',  ( -0.7071067811865355823, 0.000000000000000000, 0.7071067811865595631 ) ) ;
#9804=CARTESIAN_POINT ( 'NONE',  ( 2.000000000000000000, 1.773042676681340968, -2.276824562219559311E-15 ) ) ;
#9870=VECTOR ( 'NONE', #17346, 1000.000000000000114 ) ;
#9936=EDGE_CURVE ( 'NONE', #22150, #8400, #18232, .T. ) ;
#9937=LINE ( 'NONE', #7042, #31750 ) ;
#10004=PLANE ( 'NONE',  #33519 ) ;
#10007=CARTESIAN_POINT ( 'NONE',  ( 0.1999999999999987899, 4.286263797015736595E-16, -3.500000000000000000 ) ) ;
#10031=AXIS2_PLACEMENT_3D ( 'NONE', #25736, #26233, #15177 ) ;
#10061=AXIS2_PLACEMENT_3D ( 'NONE', #14745, #14078, #12026 ) ;
#10068=FACE_OUTER_BOUND ( 'NONE', #29734, .T. ) ;
#10073=CARTESIAN_POINT ( 'NONE',  ( 16.00000000000000000, 1.971681346627238735E-16, -1.610000000000000098 ) ) ;
#10151=DIRECTION ( 'NONE',  ( 0.000000000000000000, 0.4999999999999990008, -0.8660254037844391517 ) ) ;
#10274=DIRECTION ( 'NONE',  ( -1.000000000000000000, -0.000000000000000000, -0.000000000000000000 ) ) ;
#10295=VECTOR ( 'NONE', #13231, 1000.000000000000114 ) ;
#10320=ORIENTED_EDGE ( 'NONE', *, *, #15725, .T. ) ;
#10342=EDGE_CURVE ( 'NONE', #9697, #10890, #12379, .T. ) ;
#10426=DIRECTION ( 'NONE',  ( 0.000000000000000000, -0.5000000000000009992, -0.8660254037844380415 ) ) ;
#10428=PLANE ( 'NONE',  #30421 ) ;
#10469=CIRCLE ( 'NONE', #118, 0.2000000000000000944 ) ;
#10499=AXIS2_PLACEMENT_3D ( 'NONE', #9107, #26659, #6386 ) ;
#10524=VECTOR ( 'NONE', #25460, 1000.000000000000000 ) ;
#10535=FILL_AREA_STYLE ('',( #2700 ) ) ;
#10547=DIRECTION ( 'NONE',  ( 0.000000000000000000, 0.000000000000000000, 1.000000000000000000 ) ) ;
#10581=PRODUCT_CONTEXT ( 'NONE', #15501, 'mechanical' ) ;
#10678=CARTESIAN_POINT ( 'NONE',  ( 2.000000000000000000, 1.773042676681340968, -2.276824562219559311E-15 ) ) ;
#10688=DIRECTION ( 'NONE',  ( 0.000000000000000000, 0.000000000000000000, -1.000000000000000000 ) ) ;
#10719=VERTEX_POINT ( 'NONE', #25858 ) ;
#10725=DIRECTION ( 'NONE',  ( 1.000000000000000000, 0.000000000000000000, 0.000000000000000000 ) ) ;
#10733=CIRCLE ( 'NONE', #29763, 1.535500000000000087 ) ;
#10781=CARTESIAN_POINT ( 'NONE',  ( 2.000000000000000000, 0.8865213383406687075, -1.535500000000000975 ) ) ;
#10783=DIRECTION ( 'NONE',  ( 0.000000000000000000, 1.000000000000000000, -1.100686371591861952E-15 ) ) ;
#10784=EDGE_CURVE ( 'NONE', #2476, #24113, #13901, .T. ) ;
#10889=ORIENTED_EDGE ( 'NONE', *, *, #19928, .F. ) ;
#10890=VERTEX_POINT ( 'NONE', #5892 ) ;
#10919=DIRECTION ( 'NONE',  ( 0.000000000000000000, -1.000000000000000000, 1.100686371591861952E-15 ) ) ;
#10962=ORIENTED_EDGE ( 'NONE', *, *, #9936, .F. ) ;
#11006=MECHANICAL_DESIGN_GEOMETRIC_PRESENTATION_REPRESENTATION('',(#25276),#7835);
#11015=CARTESIAN_POINT ( 'NONE',  ( 2.000000000000000000, -0.8865213383406685965, 1.535500000000000531 ) ) ;
#11110=PLANE ( 'NONE',  #11262 ) ;
#11239=TOROIDAL_SURFACE ( 'NONE', #9607, 3.299999999999999822, 0.2000000000000000111 ) ;
#11262=AXIS2_PLACEMENT_3D ( 'NONE', #26432, #5807, #14153 ) ;
#11307=CARTESIAN_POINT ( 'NONE',  ( 0.000000000000000000, -1.773042676681340524, 1.734723475976807094E-15 ) ) ;
#11313=PLANE ( 'NONE',  #32858 ) ;
#11334=CARTESIAN_POINT ( 'NONE',  ( 2.000000000000000000, -0.8865213383406721492, -1.535499999999998977 ) ) ;
#11371=AXIS2_PLACEMENT_3D ( 'NONE', #32904, #9562, #23021 ) ;
#11384=EDGE_CURVE ( 'NONE', #5152, #28610, #21159, .T. ) ;
#11385=AXIS2_PLACEMENT_3D ( 'NONE', #21040, #8111, #5533 ) ;
#11389=EDGE_CURVE ( 'NONE', #30073, #8400, #26833, .T. ) ;
#11407=DIRECTION ( 'NONE',  ( -1.000000000000000000, -0.000000000000000000, -0.000000000000000000 ) ) ;
#11432=ADVANCED_FACE ( 'NONE', ( #5982 ), #4544, .T. ) ;
#11439=DIRECTION ( 'NONE',  ( 0.000000000000000000, 0.000000000000000000, 1.000000000000000000 ) ) ;
#11566=VECTOR ( 'NONE', #72, 1000.000000000000000 ) ;
#11594=VECTOR ( 'NONE', #14899, 1000.000000000000000 ) ;
#11640=VERTEX_POINT ( 'NONE', #22159 ) ;
#11673=PLANE ( 'NONE',  #10499 ) ;
#11734=SURFACE_SIDE_STYLE ('',( #12070 ) ) ;
#11802=LINE ( 'NONE', #22191, #21394 ) ;
#11851=ORIENTED_EDGE ( 'NONE', *, *, #10784, .T. ) ;
#11854=DIRECTION ( 'NONE',  ( 1.000000000000000000, 0.000000000000000000, 0.000000000000000000 ) ) ;
#11941=DIRECTION ( 'NONE',  ( 0.000000000000000000, 0.000000000000000000, 1.000000000000000000 ) ) ;
#11992=EDGE_LOOP ( 'NONE', ( #5753, #23591, #6133 ) ) ;
#12026=DIRECTION ( 'NONE',  ( 0.000000000000000000, 0.5000000000000009992, 0.8660254037844380415 ) ) ;
#12070=SURFACE_STYLE_FILL_AREA ( #20078 ) ;
#12082=ORIENTED_EDGE ( 'NONE', *, *, #5161, .F. ) ;
#12140=FACE_BOUND ( 'NONE', #27823, .T. ) ;
#12220=EDGE_CURVE ( 'NONE', #24113, #14984, #9937, .T. ) ;
#12243=EDGE_CURVE ( 'NONE', #16646, #9697, #31236, .T. ) ;
#12286=EDGE_CURVE ( 'NONE', #16646, #24872, #18943, .T. ) ;
#12331=ORIENTED_EDGE ( 'NONE', *, *, #3139, .F. ) ;
#12379=CIRCLE ( 'NONE', #16726, 1.535500000000000087 ) ;
#12635=EDGE_CURVE ( 'NONE', #15658, #9623, #1308, .T. ) ;
#12643=EDGE_CURVE ( 'NONE', #25501, #11640, #2947, .T. ) ;
#12646=ORIENTED_EDGE ( 'NONE', *, *, #2230, .F. ) ;
#12682=VECTOR ( 'NONE', #10426, 1000.000000000000114 ) ;
#12695=FACE_OUTER_BOUND ( 'NONE', #26016, .T. ) ;
#12725=VECTOR ( 'NONE', #26094, 1000.000000000000000 ) ;
#12743=MECHANICAL_DESIGN_GEOMETRIC_PRESENTATION_REPRESENTATION('',(#22542),#25262);
#12864=CARTESIAN_POINT ( 'NONE',  ( -31.74999999999995737, 4.286263797015736595E-16, -3.500000000000000000 ) ) ;
#12892=ORIENTED_EDGE ( 'NONE', *, *, #22246, .F. ) ;
#12954=MANIFOLD_SOLID_BREP ( 'Hex', #2552 ) ;
#12973=CARTESIAN_POINT ( 'NONE',  ( 2.000000000000000000, -0.8865213383406685965, 1.535500000000000531 ) ) ;
#12980=CIRCLE ( 'NONE', #29278, 3.299999999999999822 ) ;
#13001=CARTESIAN_POINT ( 'NONE',  ( 2.000000000000000000, -0.8865213383406685965, 1.535500000000000531 ) ) ;
#13100=CARTESIAN_POINT ( 'NONE',  ( 0.000000000000000000, 1.773042676681340968, -2.276824562219559311E-15 ) ) ;
#13110=FACE_BOUND ( 'NONE', #13350, .T. ) ;
#13179=EDGE_LOOP ( 'NONE', ( #28100, #16906, #23456, #33340 ) ) ;
#13231=DIRECTION ( 'NONE',  ( 0.000000000000000000, -0.5000000000000009992, -0.8660254037844380415 ) ) ;
#13238=AXIS2_PLACEMENT_3D ( 'NONE', #23091, #33481, #31430 ) ;
#13350=EDGE_LOOP ( 'NONE', ( #4242, #18387 ) ) ;
#13398=( LENGTH_UNIT ( ) NAMED_UNIT ( * ) SI_UNIT ( .MILLI., .METRE. ) );
#13399=DIRECTION ( 'NONE',  ( 0.000000000000000000, 0.000000000000000000, -1.000000000000000000 ) ) ;
#13440=AXIS2_PLACEMENT_3D ( 'NONE', #8385, #21990, #19269 ) ;
#13477=ADVANCED_FACE ( 'NONE', ( #30433 ), #27700, .T. ) ;
#13621=CARTESIAN_POINT ( 'NONE',  ( 4.000000000000003553, 4.286263797015736595E-16, -3.500000000000000000 ) ) ;
#13646=CARTESIAN_POINT ( 'NONE',  ( 2.000000000000000000, 0.000000000000000000, 0.000000000000000000 ) ) ;
#13692=DIRECTION ( 'NONE',  ( 0.000000000000000000, 1.224646799147353207E-16, 1.000000000000000000 ) ) ;
#13764=CARTESIAN_POINT ( 'NONE',  ( 0.000000000000000000, 0.000000000000000000, 0.000000000000000000 ) ) ;
#13858=VERTEX_POINT ( 'NONE', #33322 ) ;
#13901=LINE ( 'NONE', #16450, #27061 ) ;
#13936=DIRECTION ( 'NONE',  ( 1.000000000000000000, 0.000000000000000000, 0.000000000000000000 ) ) ;
#13940=AXIS2_PLACEMENT_3D ( 'NONE', #10781, #19056, #1163 ) ;
#13965=CARTESIAN_POINT ( 'NONE',  ( 2.000000000000000000, 1.773042676681340968, -2.276824562219559311E-15 ) ) ;
#14078=DIRECTION ( 'NONE',  ( 0.000000000000000000, 0.8660254037844380415, -0.5000000000000009992 ) ) ;
#14117=CARTESIAN_POINT ( 'NONE',  ( 2.000000000000000000, 0.8865213383406687075, -1.535500000000000975 ) ) ;
#14153=DIRECTION ( 'NONE',  ( 0.000000000000000000, 0.000000000000000000, -1.000000000000000000 ) ) ;
#14178=ADVANCED_FACE ( 'NONE', ( #22877 ), #5534, .F. ) ;
#14231=ORIENTED_EDGE ( 'NONE', *, *, #12635, .T. ) ;
#14267=DIRECTION ( 'NONE',  ( 0.000000000000000000, 0.000000000000000000, 1.000000000000000000 ) ) ;
#14306=AXIS2_PLACEMENT_3D ( 'NONE', #8358, #3739, #18748 ) ;
#14312=AXIS2_PLACEMENT_3D ( 'NONE', #23395, #7564, #20829 ) ;
#14502=DIRECTION ( 'NONE',  ( -1.000000000000000000, -0.000000000000000000, -0.000000000000000000 ) ) ;
#14517=ORIENTED_EDGE ( 'NONE', *, *, #31606, .F. ) ;
#14520=PLANE ( 'NONE',  #23576 ) ;
#14593=CIRCLE ( 'NONE', #5357, 1.535500000000000087 ) ;
#14610=DIRECTION ( 'NONE',  ( 0.000000000000000000, 0.000000000000000000, 1.000000000000000000 ) ) ;
#14651=ORIENTED_EDGE ( 'NONE', *, *, #31606, .T. ) ;
#14676=CYLINDRICAL_SURFACE ( 'NONE', #11371, 2.000000000000000888 ) ;
#14711=EDGE_LOOP ( 'NONE', ( #25632, #32836, #25712 ) ) ;
#14745=CARTESIAN_POINT ( 'NONE',  ( 2.000000000000000000, -0.8865213383406685965, 1.535500000000000531 ) ) ;
#14754=LINE ( 'NONE', #4543, #17195 ) ;
#14853=ORIENTED_EDGE ( 'NONE', *, *, #21057, .F. ) ;
#14870=PRODUCT ( 'socket head cap screw_iso_ISO 4762 M4 x 12 - 12N', 'socket head cap screw_iso_ISO 4762 M4 x 12 - 12N', '', ( #10581 ) ) ;
#14899=DIRECTION ( 'NONE',  ( -0.5000000000000061062, 1.060575238724902601E-16, -0.8660254037844351549 ) ) ;
#14900=VECTOR ( 'NONE', #26767, 1000.000000000000000 ) ;
#14902=CARTESIAN_POINT ( 'NONE',  ( 16.00000000000000000, 0.000000000000000000, 1.610000000000000098 ) ) ;
#14933=FACE_OUTER_BOUND ( 'NONE', #17664, .T. ) ;
#14984=VERTEX_POINT ( 'NONE', #25310 ) ;
#15035=DIRECTION ( 'NONE',  ( -1.000000000000000000, -0.000000000000000000, -0.000000000000000000 ) ) ;
#15076=CARTESIAN_POINT ( 'NONE',  ( 0.1999999999999987899, 0.000000000000000000, 0.000000000000000000 ) ) ;
#15138=AXIS2_PLACEMENT_3D ( 'NONE', #15187, #18034, #10547 ) ;
#15177=DIRECTION ( 'NONE',  ( 0.000000000000000000, 0.000000000000000000, 1.000000000000000000 ) ) ;
#15186=CARTESIAN_POINT ( 'NONE',  ( 15.61000000000001364, 2.449293598294707400E-16, -2.000000000000000888 ) ) ;
#15187=CARTESIAN_POINT ( 'NONE',  ( -31.74999999999995737, 0.000000000000000000, 0.000000000000000000 ) ) ;
#15195=ORIENTED_EDGE ( 'NONE', *, *, #1070, .F. ) ;
#15219=DIRECTION ( 'NONE',  ( 0.000000000000000000, 0.4999999999999991118, -0.8660254037844391517 ) ) ;
#15417=LINE ( 'NONE', #7417, #24319 ) ;
#15483=FACE_OUTER_BOUND ( 'NONE', #11992, .T. ) ;
#15501=APPLICATION_CONTEXT ( 'automotive_design' ) ;
#15655=ORIENTED_EDGE ( 'NONE', *, *, #33042, .F. ) ;
#15658=VERTEX_POINT ( 'NONE', #30915 ) ;
#15725=EDGE_CURVE ( 'NONE', #16822, #6483, #6686, .T. ) ;
#15758=EDGE_CURVE ( 'NONE', #16822, #11640, #4495, .T. ) ;
#15761=FACE_OUTER_BOUND ( 'NONE', #21844, .T. ) ;
#15793=( NAMED_UNIT ( * ) PLANE_ANGLE_UNIT ( ) SI_UNIT ( $, .RADIAN. ) );
#15827=EDGE_CURVE ( 'NONE', #2182, #6483, #31083, .T. ) ;
#15883=CARTESIAN_POINT ( 'NONE',  ( 2.000000000000000000, 1.773042676681340968, -2.276824562219559311E-15 ) ) ;
#15884=CARTESIAN_POINT ( 'NONE',  ( 0.000000000000000000, -0.8865213383406685965, 1.535500000000000531 ) ) ;
#15899=CARTESIAN_POINT ( 'NONE',  ( 2.000000000000000000, 0.000000000000000000, 0.000000000000000000 ) ) ;
#15941=ORIENTED_EDGE ( 'NONE', *, *, #25545, .F. ) ;
#15959=( NAMED_UNIT ( * ) SI_UNIT ( $, .STERADIAN. ) SOLID_ANGLE_UNIT ( ) );
#16058=ORIENTED_EDGE ( 'NONE', *, *, #21057, .T. ) ;
#16149=CARTESIAN_POINT ( 'NONE',  ( 2.000000000000000000, 0.000000000000000000, 0.000000000000000000 ) ) ;
#16186=EDGE_LOOP ( 'NONE', ( #7205, #29985, #25374, #32024, #31692 ) ) ;
#16221=VECTOR ( 'NONE', #10151, 1000.000000000000227 ) ;
#16259=CARTESIAN_POINT ( 'NONE',  ( 4.200000000000001954, 2.694222958124178486E-16, 2.200000000000001066 ) ) ;
#16263=DIRECTION ( 'NONE',  ( -1.000000000000000000, -0.000000000000000000, -0.000000000000000000 ) ) ;
#16371=DIRECTION ( 'NONE',  ( -1.000000000000000000, -0.000000000000000000, -0.000000000000000000 ) ) ;
#16401=EDGE_CURVE ( 'NONE', #31219, #25762, #20299, .T. ) ;
#16409=CARTESIAN_POINT ( 'NONE',  ( 2.000000000000000000, 0.000000000000000000, 0.000000000000000000 ) ) ;
#16436=PRODUCT_DEFINITION_FORMATION_WITH_SPECIFIED_SOURCE ( 'ANY', '', #14870, .NOT_KNOWN. ) ;
#16450=CARTESIAN_POINT ( 'NONE',  ( 2.000000000000000000, -0.8865213383406685965, 1.535500000000000531 ) ) ;
#16456=VECTOR ( 'NONE', #28750, 1000.000000000000000 ) ;
#16487=FACE_OUTER_BOUND ( 'NONE', #2798, .T. ) ;
#16562=ORIENTED_EDGE ( 'NONE', *, *, #15827, .F. ) ;
#16604=ORIENTED_EDGE ( 'NONE', *, *, #12643, .T. ) ;
#16646=VERTEX_POINT ( 'NONE', #13965 ) ;
#16659=ORIENTED_EDGE ( 'NONE', *, *, #33256, .T. ) ;
#16660=CIRCLE ( 'NONE', #23749, 2.000000000000000888 ) ;
#16694=CARTESIAN_POINT ( 'NONE',  ( 0.000000000000000000, 1.773042676681340968, -2.276824562219559311E-15 ) ) ;
#16726=AXIS2_PLACEMENT_3D ( 'NONE', #4053, #17343, #9170 ) ;
#16739=ORIENTED_EDGE ( 'NONE', *, *, #1292, .F. ) ;
#16822=VERTEX_POINT ( 'NONE', #10007 ) ;
#16833=PLANE ( 'NONE',  #13940 ) ;
#16838=DIRECTION ( 'NONE',  ( -1.000000000000000000, -0.000000000000000000, -0.000000000000000000 ) ) ;
#16898=ORIENTED_EDGE ( 'NONE', *, *, #19928, .T. ) ;
#16906=ORIENTED_EDGE ( 'NONE', *, *, #9936, .T. ) ;
#17009=FILL_AREA_STYLE_COLOUR ( '', #4599 ) ;
#17065=VECTOR ( 'NONE', #7899, 1000.000000000000114 ) ;
#17086=CARTESIAN_POINT ( 'NONE',  ( 2.000000000000000000, 1.773042676681340968, -2.276824562219559311E-15 ) ) ;
#17195=VECTOR ( 'NONE', #1987, 1000.000000000000114 ) ;
#17216=EDGE_CURVE ( 'NONE', #23772, #10719, #21719, .T. ) ;
#17247=ADVANCED_FACE ( 'NONE', ( #27173 ), #11673, .T. ) ;
#17343=DIRECTION ( 'NONE',  ( -1.000000000000000000, -0.000000000000000000, -0.000000000000000000 ) ) ;
#17346=DIRECTION ( 'NONE',  ( 0.000000000000000000, -0.5000000000000011102, -0.8660254037844379305 ) ) ;
#17447=ORIENTED_EDGE ( 'NONE', *, *, #1692, .F. ) ;
#17458=LINE ( 'NONE', #14902, #18393 ) ;
#17658=DIRECTION ( 'NONE',  ( 1.000000000000000000, 0.000000000000000000, 0.000000000000000000 ) ) ;
#17664=EDGE_LOOP ( 'NONE', ( #4935, #24918, #15941 ) ) ;
#17712=EDGE_CURVE ( 'NONE', #6185, #10719, #31415, .T. ) ;
#17798=ORIENTED_EDGE ( 'NONE', *, *, #20196, .F. ) ;
#17822=DIRECTION ( 'NONE',  ( 0.000000000000000000, 0.000000000000000000, -1.000000000000000000 ) ) ;
#17842=EDGE_CURVE ( 'NONE', #25762, #23772, #2293, .T. ) ;
#17849=EDGE_CURVE ( 'NONE', #25762, #14984, #30650, .T. ) ;
#17890=EDGE_LOOP ( 'NONE', ( #3402, #24944, #14651, #17447 ) ) ;
#18010=ORIENTED_EDGE ( 'NONE', *, *, #30102, .F. ) ;
#18034=DIRECTION ( 'NONE',  ( -1.000000000000000000, -0.000000000000000000, -0.000000000000000000 ) ) ;
#18059=EDGE_LOOP ( 'NONE', ( #18010, #10 ) ) ;
#18073=DIRECTION ( 'NONE',  ( 0.000000000000000000, 0.000000000000000000, -1.000000000000000000 ) ) ;
#18149=AXIS2_PLACEMENT_3D ( 'NONE', #1381, #16371, #26939 ) ;
#18197=CONICAL_SURFACE ( 'NONE', #27372, 1.610000000000000098, 0.7853981633974652654 ) ;
#18232=LINE ( 'NONE', #10073, #18889 ) ;
#18319=ADVANCED_FACE ( 'NONE', ( #8284 ), #7958, .F. ) ;
#18358=( NAMED_UNIT ( * ) SI_UNIT ( $, .STERADIAN. ) SOLID_ANGLE_UNIT ( ) );
#18387=ORIENTED_EDGE ( 'NONE', *, *, #22179, .T. ) ;
#18393=VECTOR ( 'NONE', #9799, 1000.000000000000114 ) ;
#18398=CIRCLE ( 'NONE', #25445, 1.610000000000000098 ) ;
#18519=DIRECTION ( 'NONE',  ( -1.000000000000000000, -0.000000000000000000, -0.000000000000000000 ) ) ;
#18552=EDGE_CURVE ( 'NONE', #29718, #25762, #7074, .T. ) ;
#18558=EDGE_CURVE ( 'NONE', #5848, #4155, #30751, .T. ) ;
#18644=DIRECTION ( 'NONE',  ( 1.000000000000000000, 0.000000000000000000, 0.000000000000000000 ) ) ;
#18671=DIRECTION ( 'NONE',  ( 1.000000000000000000, 0.000000000000000000, 0.000000000000000000 ) ) ;
#18740=CARTESIAN_POINT ( 'NONE',  ( 0.000000000000000000, 0.8865213383406687075, -1.535500000000000975 ) ) ;
#18748=DIRECTION ( 'NONE',  ( 0.000000000000000000, 0.000000000000000000, 1.000000000000000000 ) ) ;
#18820=CARTESIAN_POINT ( 'NONE',  ( 15.61000000000001364, 0.000000000000000000, 2.000000000000000888 ) ) ;
#18823=AXIS2_PLACEMENT_3D ( 'NONE', #4881, #20044, #28046 ) ;
#18831=EDGE_CURVE ( 'NONE', #5170, #10719, #3129, .T. ) ;
#18889=VECTOR ( 'NONE', #20450, 1000.000000000000114 ) ;
#18943=LINE ( 'NONE', #19278, #14900 ) ;
#18997=CARTESIAN_POINT ( 'NONE',  ( 2.000000000000000000, 0.000000000000000000, 1.535500000000000087 ) ) ;
#19056=DIRECTION ( 'NONE',  ( 0.000000000000000000, -1.222984857324291014E-15, -1.000000000000000000 ) ) ;
#19205=AXIS2_PLACEMENT_3D ( 'NONE', #15899, #30920, #28688 ) ;
#19229=VECTOR ( 'NONE', #23417, 1000.000000000000000 ) ;
#19238=CARTESIAN_POINT ( 'NONE',  ( 2.000000000000000000, 1.690103923579303787E-15, 1.535499999999999865 ) ) ;
#19269=DIRECTION ( 'NONE',  ( 0.000000000000000000, 0.000000000000000000, 1.000000000000000000 ) ) ;
#19278=CARTESIAN_POINT ( 'NONE',  ( 2.000000000000000000, 1.773042676681340968, -2.276824562219559311E-15 ) ) ;
#19337=ORIENTED_EDGE ( 'NONE', *, *, #33256, .F. ) ;
#19426=VECTOR ( 'NONE', #648, 1000.000000000000114 ) ;
#19509=CIRCLE ( 'NONE', #1033, 3.500000000000000000 ) ;
#19651=DIRECTION ( 'NONE',  ( -1.000000000000000000, -0.000000000000000000, -0.000000000000000000 ) ) ;
#19870=CARTESIAN_POINT ( 'NONE',  ( 16.00000000000000000, 2.210487472460973191E-16, -1.610000000000000098 ) ) ;
#19878=EDGE_LOOP ( 'NONE', ( #25850, #16659, #10320, #16562 ) ) ;
#19887=VERTEX_POINT ( 'NONE', #9535 ) ;
#19925=EDGE_LOOP ( 'NONE', ( #6260, #9285, #30071, #11851, #16058 ) ) ;
#19928=EDGE_CURVE ( 'NONE', #28610, #19887, #24871, .T. ) ;
#19955=CARTESIAN_POINT ( 'NONE',  ( 2.000000000000000000, 0.000000000000000000, 0.000000000000000000 ) ) ;
#20024=DIRECTION ( 'NONE',  ( 0.000000000000000000, 0.000000000000000000, 1.000000000000000000 ) ) ;
#20044=DIRECTION ( 'NONE',  ( -1.000000000000000000, -0.000000000000000000, -0.000000000000000000 ) ) ;
#20078=FILL_AREA_STYLE ('',( #17009 ) ) ;
#20143=DIRECTION ( 'NONE',  ( -0.000000000000000000, 0.000000000000000000, 1.000000000000000000 ) ) ;
#20196=EDGE_CURVE ( 'NONE', #16646, #10890, #7838, .T. ) ;
#20231=ORIENTED_EDGE ( 'NONE', *, *, #11384, .F. ) ;
#20299=LINE ( 'NONE', #25409, #12725 ) ;
#20310=AXIS2_PLACEMENT_3D ( 'NONE', #9760, #32920, #20143 ) ;
#20407=CARTESIAN_POINT ( 'NONE',  ( 2.000000000000000000, 1.773042676681340968, -2.276824562219559311E-15 ) ) ;
#20409=ORIENTED_EDGE ( 'NONE', *, *, #20196, .T. ) ;
#20450=DIRECTION ( 'NONE',  ( -0.7071067811865355823, 8.659560562355079537E-17, -0.7071067811865595631 ) ) ;
#20532=CARTESIAN_POINT ( 'NONE',  ( 2.000000000000000000, -1.773042676681340524, 1.734723475976807094E-15 ) ) ;
#20573=DIRECTION ( 'NONE',  ( 0.000000000000000000, -0.5000000000000011102, -0.8660254037844379305 ) ) ;
#20609=ORIENTED_EDGE ( 'NONE', *, *, #18558, .T. ) ;
#20681=ORIENTED_EDGE ( 'NONE', *, *, #26611, .F. ) ;
#20785=ADVANCED_FACE ( 'NONE', ( #1658 ), #18197, .T. ) ;
#20800=CARTESIAN_POINT ( 'NONE',  ( 4.000000000000001776, 0.000000000000000000, -2.200000000000001066 ) ) ;
#20829=DIRECTION ( 'NONE',  ( 0.000000000000000000, 0.000000000000000000, 1.000000000000000000 ) ) ;
#20849=AXIS2_PLACEMENT_3D ( 'NONE', #8135, #18519, #5558 ) ;
#20910=LINE ( 'NONE', #20407, #23259 ) ;
#21040=CARTESIAN_POINT ( 'NONE',  ( 4.200000000000001954, 0.000000000000000000, 0.000000000000000000 ) ) ;
#21046=ADVANCED_FACE ( 'NONE', ( #23790 ), #14520, .F. ) ;
#21056=PRODUCT_DEFINITION ( 'UNKNOWN', '', #16436, #3959 ) ;
#21057=EDGE_CURVE ( 'NONE', #24113, #6185, #11802, .T. ) ;
#21150=ORIENTED_EDGE ( 'NONE', *, *, #21202, .T. ) ;
#21159=LINE ( 'NONE', #13001, #26286 ) ;
#21202=EDGE_CURVE ( 'NONE', #8400, #30073, #7258, .T. ) ;
#21274=ORIENTED_EDGE ( 'NONE', *, *, #12286, .F. ) ;
#21346=CARTESIAN_POINT ( 'NONE',  ( 0.000000000000000000, 0.8865213383406687075, -1.535500000000000975 ) ) ;
#21364=ADVANCED_FACE ( 'NONE', ( #12140, #30539 ), #25422, .T. ) ;
#21394=VECTOR ( 'NONE', #23956, 1000.000000000000000 ) ;
#21475=ORIENTED_EDGE ( 'NONE', *, *, #23673, .T. ) ;
#21521=CARTESIAN_POINT ( 'NONE',  ( 2.000000000000000000, -0.8865213383406685965, 1.535500000000000531 ) ) ;
#21539=LINE ( 'NONE', #18997, #3638 ) ;
#21562=DIRECTION ( 'NONE',  ( 0.000000000000000000, -0.5000000000000009992, -0.8660254037844380415 ) ) ;
#21719=LINE ( 'NONE', #11334, #30623 ) ;
#21729=ORIENTED_EDGE ( 'NONE', *, *, #15758, .F. ) ;
#21775=ADVANCED_BREP_SHAPE_REPRESENTATION ( '', ( #12954, #2404 ), #1885 ) ;
#21844=EDGE_LOOP ( 'NONE', ( #23902, #31905, #12082, #16739 ) ) ;
#21990=DIRECTION ( 'NONE',  ( -1.000000000000000000, -0.000000000000000000, -0.000000000000000000 ) ) ;
#22087=ADVANCED_FACE ( 'NONE', ( #14933 ), #10004, .F. ) ;
#22101=ORIENTED_EDGE ( 'NONE', *, *, #23673, .F. ) ;
#22121=SURFACE_STYLE_USAGE ( .BOTH. , #11734 ) ;
#22150=VERTEX_POINT ( 'NONE', #19870 ) ;
#22159=CARTESIAN_POINT ( 'NONE',  ( 0.000000000000000000, 4.163799117101000559E-16, -3.299999999999999822 ) ) ;
#22175=SHAPE_REPRESENTATION ( 'socket head cap screw_iso_ISO 4762 M4 x 12 - 12N', ( #2404 ), #1885 ) ;
#22179=EDGE_CURVE ( 'NONE', #25924, #30416, #27598, .T. ) ;
#22191=CARTESIAN_POINT ( 'NONE',  ( 2.000000000000000000, -1.773042676681340524, 1.734723475976807094E-15 ) ) ;
#22246=EDGE_CURVE ( 'NONE', #9697, #28610, #14754, .T. ) ;
#22542=STYLED_ITEM ( 'NONE', ( #30134 ), #12954 ) ;
#22545=FACE_OUTER_BOUND ( 'NONE', #19878, .T. ) ;
#22670=CIRCLE ( 'NONE', #4694, 3.500000000000000000 ) ;
#22748=DIRECTION ( 'NONE',  ( 0.000000000000000000, 0.000000000000000000, -1.000000000000000000 ) ) ;
#22802=EDGE_CURVE ( 'NONE', #32112, #2182, #22670, .T. ) ;
#22836=CARTESIAN_POINT ( 'NONE',  ( 4.000000000000003553, 0.000000000000000000, 3.500000000000000000 ) ) ;
#22877=FACE_OUTER_BOUND ( 'NONE', #16186, .T. ) ;
#22912=ADVANCED_FACE ( 'NONE', ( #33252 ), #11239, .T. ) ;
#22922=AXIS2_PLACEMENT_3D ( 'NONE', #30555, #7391, #15219 ) ;
#22955=AXIS2_PLACEMENT_3D ( 'NONE', #2778, #15035, #33268 ) ;
#22981=ORIENTED_EDGE ( 'NONE', *, *, #4756, .T. ) ;
#23021=DIRECTION ( 'NONE',  ( 0.000000000000000000, 0.000000000000000000, 1.000000000000000000 ) ) ;
#23083=VECTOR ( 'NONE', #6990, 1000.000000000000000 ) ;
#23091=CARTESIAN_POINT ( 'NONE',  ( -31.74999999999995737, 0.000000000000000000, 0.000000000000000000 ) ) ;
#23190=CARTESIAN_POINT ( 'NONE',  ( 0.000000000000000000, -0.8865213383406685965, 1.535500000000000531 ) ) ;
#23207=ORIENTED_EDGE ( 'NONE', *, *, #7291, .F. ) ;
#23259=VECTOR ( 'NONE', #20573, 1000.000000000000114 ) ;
#23302=LINE ( 'NONE', #27148, #16456 ) ;
#23395=CARTESIAN_POINT ( 'NONE',  ( 15.61000000000001364, 0.000000000000000000, 0.000000000000000000 ) ) ;
#23409=CARTESIAN_POINT ( 'NONE',  ( -31.74999999999995737, 0.000000000000000000, 3.500000000000000000 ) ) ;
#23417=DIRECTION ( 'NONE',  ( 0.000000000000000000, -1.000000000000000000, 1.222984857324291014E-15 ) ) ;
#23453=EDGE_LOOP ( 'NONE', ( #25278, #8663, #2837, #26292 ) ) ;
#23456=ORIENTED_EDGE ( 'NONE', *, *, #11389, .F. ) ;
#23575=DIRECTION ( 'NONE',  ( -0.000000000000000000, 1.000000000000000000, 1.224646799147353207E-16 ) ) ;
#23576=AXIS2_PLACEMENT_3D ( 'NONE', #17086, #9248, #24758 ) ;
#23584=AXIS2_PLACEMENT_3D ( 'NONE', #15076, #11854, #20024 ) ;
#23591=ORIENTED_EDGE ( 'NONE', *, *, #16401, .T. ) ;
#23673=EDGE_CURVE ( 'NONE', #24872, #19887, #23986, .T. ) ;
#23738=ORIENTED_EDGE ( 'NONE', *, *, #1282, .T. ) ;
#23749=AXIS2_PLACEMENT_3D ( 'NONE', #5238, #25859, #13399 ) ;
#23772=VERTEX_POINT ( 'NONE', #3865 ) ;
#23790=FACE_OUTER_BOUND ( 'NONE', #31853, .T. ) ;
#23877=FACE_OUTER_BOUND ( 'NONE', #13179, .T. ) ;
#23902=ORIENTED_EDGE ( 'NONE', *, *, #12635, .F. ) ;
#23906=CONICAL_SURFACE ( 'NONE', #32075, 1.535500000000000087, 1.047197551196590748 ) ;
#23931=DIRECTION ( 'NONE',  ( 0.000000000000000000, 1.000000000000000000, -1.224646799147353207E-16 ) ) ;
#23950=CARTESIAN_POINT ( 'NONE',  ( 2.000000000000000000, -1.773042676681340524, 1.734723475976807094E-15 ) ) ;
#23956=DIRECTION ( 'NONE',  ( -1.000000000000000000, -0.000000000000000000, -0.000000000000000000 ) ) ;
#23957=UNCERTAINTY_MEASURE_WITH_UNIT (LENGTH_MEASURE( 1.000000000000000082E-05 ), #24849, 'distance_accuracy_value', 'NONE');
#23986=LINE ( 'NONE', #13100, #19426 ) ;
#24113=VERTEX_POINT ( 'NONE', #23950 ) ;
#24319=VECTOR ( 'NONE', #4859, 1000.000000000000000 ) ;
#24495=DIRECTION ( 'NONE',  ( 1.000000000000000000, 0.000000000000000000, 0.000000000000000000 ) ) ;
#24518=EDGE_CURVE ( 'NONE', #13858, #30073, #17458, .T. ) ;
#24647=PRODUCT_DEFINITION_SHAPE ( 'NONE', 'NONE',  #21056 ) ;
#24700=ORIENTED_EDGE ( 'NONE', *, *, #10784, .F. ) ;
#24706=AXIS2_PLACEMENT_3D ( 'NONE', #2577, #28123, #18073 ) ;
#24758=DIRECTION ( 'NONE',  ( 0.000000000000000000, 0.5000000000000011102, 0.8660254037844379305 ) ) ;
#24766=CYLINDRICAL_SURFACE ( 'NONE', #31437, 3.500000000000000000 ) ;
#24849=( LENGTH_UNIT ( ) NAMED_UNIT ( * ) SI_UNIT ( .MILLI., .METRE. ) );
#24865=VECTOR ( 'NONE', #16838, 1000.000000000000000 ) ;
#24871=LINE ( 'NONE', #30159, #23083 ) ;
#24872=VERTEX_POINT ( 'NONE', #16694 ) ;
#24918=ORIENTED_EDGE ( 'NONE', *, *, #26611, .T. ) ;
#24944=ORIENTED_EDGE ( 'NONE', *, *, #31847, .T. ) ;
#24993=CARTESIAN_POINT ( 'NONE',  ( 2.000000000000000000, 1.773042676681340968, -2.276824562219559311E-15 ) ) ;
#25006=CARTESIAN_POINT ( 'NONE',  ( 16.00000000000000000, 0.000000000000000000, 0.000000000000000000 ) ) ;
#25262=( GEOMETRIC_REPRESENTATION_CONTEXT ( 3 ) GLOBAL_UNCERTAINTY_ASSIGNED_CONTEXT ( ( #23957 ) ) GLOBAL_UNIT_ASSIGNED_CONTEXT ( ( #24849, #25352, #9684 ) ) REPRESENTATION_CONTEXT ( 'NONE', 'WORKASPACE' ) );
#25276=STYLED_ITEM ( 'NONE', ( #5727 ), #21775 ) ;
#25278=ORIENTED_EDGE ( 'NONE', *, *, #15725, .F. ) ;
#25297=APPLICATION_CONTEXT ( 'automotive_design' ) ;
#25310=CARTESIAN_POINT ( 'NONE',  ( 2.000000000000000000, -1.329782007511006281, -0.7677499999999984892 ) ) ;
#25352=( NAMED_UNIT ( * ) PLANE_ANGLE_UNIT ( ) SI_UNIT ( $, .RADIAN. ) );
#25374=ORIENTED_EDGE ( 'NONE', *, *, #17849, .T. ) ;
#25409=CARTESIAN_POINT ( 'NONE',  ( 2.000000000000000000, 0.8865213383406687075, -1.535500000000000975 ) ) ;
#25422=PLANE ( 'NONE',  #20310 ) ;
#25445=AXIS2_PLACEMENT_3D ( 'NONE', #3339, #29577, #3674 ) ;
#25460=DIRECTION ( 'NONE',  ( -1.000000000000000000, -0.000000000000000000, -0.000000000000000000 ) ) ;
#25498=CIRCLE ( 'NONE', #30963, 1.610000000000000098 ) ;
#25501=VERTEX_POINT ( 'NONE', #321 ) ;
#25545=EDGE_CURVE ( 'NONE', #2476, #5152, #14593, .T. ) ;
#25552=ORIENTED_EDGE ( 'NONE', *, *, #17712, .T. ) ;
#25603=EDGE_CURVE ( 'NONE', #11640, #25501, #12980, .T. ) ;
#25632=ORIENTED_EDGE ( 'NONE', *, *, #17842, .T. ) ;
#25635=ADVANCED_FACE ( 'NONE', ( #9496 ), #30112, .F. ) ;
#25710=ORIENTED_EDGE ( 'NONE', *, *, #22179, .F. ) ;
#25712=ORIENTED_EDGE ( 'NONE', *, *, #17849, .F. ) ;
#25736=CARTESIAN_POINT ( 'NONE',  ( 0.000000000000000000, 0.000000000000000000, 0.000000000000000000 ) ) ;
#25762=VERTEX_POINT ( 'NONE', #6262 ) ;
#25831=CARTESIAN_POINT ( 'NONE',  ( 2.886521338340684917, 4.440929409521844457E-17, 0.000000000000000000 ) ) ;
#25850=ORIENTED_EDGE ( 'NONE', *, *, #2230, .T. ) ;
#25858=CARTESIAN_POINT ( 'NONE',  ( 0.000000000000000000, -0.8865213383406721492, -1.535499999999998977 ) ) ;
#25859=DIRECTION ( 'NONE',  ( 1.000000000000000000, 0.000000000000000000, 0.000000000000000000 ) ) ;
#25924=VERTEX_POINT ( 'NONE', #30457 ) ;
#26016=EDGE_LOOP ( 'NONE', ( #31003, #21150, #2729, #14231 ) ) ;
#26035=AXIS2_PLACEMENT_3D ( 'NONE', #32660, #24495, #3874 ) ;
#26094=DIRECTION ( 'NONE',  ( 0.000000000000000000, -1.000000000000000000, 1.222984857324291014E-15 ) ) ;
#26108=ORIENTED_EDGE ( 'NONE', *, *, #22802, .T. ) ;
#26233=DIRECTION ( 'NONE',  ( -1.000000000000000000, -0.000000000000000000, -0.000000000000000000 ) ) ;
#26240=EDGE_CURVE ( 'NONE', #5848, #2476, #28901, .T. ) ;
#26286=VECTOR ( 'NONE', #10783, 1000.000000000000000 ) ;
#26289=AXIS2_PLACEMENT_3D ( 'NONE', #10678, #18671, #29063 ) ;
#26292=ORIENTED_EDGE ( 'NONE', *, *, #4756, .F. ) ;
#26297=EDGE_LOOP ( 'NONE', ( #6781, #14853, #33455, #28099, #7196 ) ) ;
#26326=CARTESIAN_POINT ( 'NONE',  ( 16.00000000000000000, 0.000000000000000000, 0.000000000000000000 ) ) ;
#26412=FACE_OUTER_BOUND ( 'NONE', #905, .T. ) ;
#26424=ORIENTED_EDGE ( 'NONE', *, *, #26625, .T. ) ;
#26432=CARTESIAN_POINT ( 'NONE',  ( 2.000000000000000000, 1.773042676681340968, -2.276824562219559311E-15 ) ) ;
#26540=DIRECTION ( 'NONE',  ( 0.000000000000000000, 0.000000000000000000, 1.000000000000000000 ) ) ;
#26611=EDGE_CURVE ( 'NONE', #5848, #5152, #33309, .T. ) ;
#26625=EDGE_CURVE ( 'NONE', #4155, #19887, #15417, .T. ) ;
#26653=DIRECTION ( 'NONE',  ( -0.5000000000000061062, 0.000000000000000000, 0.8660254037844351549 ) ) ;
#26659=DIRECTION ( 'NONE',  ( -0.000000000000000000, 0.8660254037844391517, 0.4999999999999990563 ) ) ;
#26767=DIRECTION ( 'NONE',  ( -1.000000000000000000, -0.000000000000000000, -0.000000000000000000 ) ) ;
#26781=ORIENTED_EDGE ( 'NONE', *, *, #33042, .T. ) ;
#26822=ORIENTED_EDGE ( 'NONE', *, *, #10342, .T. ) ;
#26833=CIRCLE ( 'NONE', #14312, 2.000000000000000888 ) ;
#26838=ORIENTED_EDGE ( 'NONE', *, *, #24518, .T. ) ;
#26921=EDGE_LOOP ( 'NONE', ( #16604, #33678 ) ) ;
#26939=DIRECTION ( 'NONE',  ( 0.000000000000000000, 0.000000000000000000, 1.000000000000000000 ) ) ;
#26985=EDGE_CURVE ( 'NONE', #31219, #5170, #1673, .T. ) ;
#27005=ORIENTED_EDGE ( 'NONE', *, *, #26625, .F. ) ;
#27061=VECTOR ( 'NONE', #21562, 1000.000000000000114 ) ;
#27145=EDGE_LOOP ( 'NONE', ( #21729, #15655, #22981, #391 ) ) ;
#27148=CARTESIAN_POINT ( 'NONE',  ( -31.74999999999995737, 2.449293598294707893E-16, -2.000000000000000888 ) ) ;
#27173=FACE_OUTER_BOUND ( 'NONE', #26297, .T. ) ;
#27372=AXIS2_PLACEMENT_3D ( 'NONE', #25006, #4386, #14610 ) ;
#27598=CIRCLE ( 'NONE', #18823, 2.200000000000001066 ) ;
#27616=FACE_OUTER_BOUND ( 'NONE', #17890, .T. ) ;
#27700=PLANE ( 'NONE',  #10061 ) ;
#27781=CARTESIAN_POINT ( 'NONE',  ( 0.1999999999999987899, 0.000000000000000000, 3.299999999999999822 ) ) ;
#27809=DIRECTION ( 'NONE',  ( 0.000000000000000000, 0.4999999999999990008, -0.8660254037844391517 ) ) ;
#27823=EDGE_LOOP ( 'NONE', ( #21475, #27005, #7586, #25552, #4644, #12331 ) ) ;
#27943=CARTESIAN_POINT ( 'NONE',  ( 4.200000000000001954, 2.449293598294707893E-16, -2.000000000000000888 ) ) ;
#28046=DIRECTION ( 'NONE',  ( 0.000000000000000000, 0.000000000000000000, -1.000000000000000000 ) ) ;
#28099=ORIENTED_EDGE ( 'NONE', *, *, #1631, .T. ) ;
#28100=ORIENTED_EDGE ( 'NONE', *, *, #30102, .T. ) ;
#28123=DIRECTION ( 'NONE',  ( 1.000000000000000000, 0.000000000000000000, 0.000000000000000000 ) ) ;
#28143=ORIENTED_EDGE ( 'NONE', *, *, #9364, .T. ) ;
#28177=AXIS2_PLACEMENT_3D ( 'NONE', #8298, #3013, #10688 ) ;
#28200=CARTESIAN_POINT ( 'NONE',  ( 2.000000000000000000, -0.8865213383406685965, 1.535500000000000531 ) ) ;
#28266=PLANE ( 'NONE',  #7803 ) ;
#28283=CARTESIAN_POINT ( 'NONE',  ( 2.000000000000000000, 1.773042676681340968, -2.276824562219559311E-15 ) ) ;
#28368=FACE_OUTER_BOUND ( 'NONE', #31254, .T. ) ;
#28475=LINE ( 'NONE', #23190, #12682 ) ;
#28548=LINE ( 'NONE', #12864, #6151 ) ;
#28586=SURFACE_SIDE_STYLE ('',( #795 ) ) ;
#28610=VERTEX_POINT ( 'NONE', #31195 ) ;
#28682=CARTESIAN_POINT ( 'NONE',  ( 0.1999999999999987899, 0.000000000000000000, 0.000000000000000000 ) ) ;
#28688=DIRECTION ( 'NONE',  ( 0.000000000000000000, 0.000000000000000000, 1.000000000000000000 ) ) ;
#28705=LINE ( 'NONE', #30765, #2673 ) ;
#28733=CIRCLE ( 'NONE', #28177, 0.2000000000000000944 ) ;
#28750=DIRECTION ( 'NONE',  ( -1.000000000000000000, -0.000000000000000000, -0.000000000000000000 ) ) ;
#28833=FACE_OUTER_BOUND ( 'NONE', #30160, .T. ) ;
#28901=LINE ( 'NONE', #11015, #10295 ) ;
#29063=DIRECTION ( 'NONE',  ( 0.000000000000000000, 0.000000000000000000, -1.000000000000000000 ) ) ;
#29102=ORIENTED_EDGE ( 'NONE', *, *, #33659, .F. ) ;
#29243=SURFACE_STYLE_USAGE ( .BOTH. , #28586 ) ;
#29278=AXIS2_PLACEMENT_3D ( 'NONE', #13764, #30280, #14267 ) ;
#29313=ADVANCED_FACE ( 'NONE', ( #7652 ), #5420, .T. ) ;
#29485=ORIENTED_EDGE ( 'NONE', *, *, #9276, .T. ) ;
#29577=DIRECTION ( 'NONE',  ( -1.000000000000000000, -0.000000000000000000, -0.000000000000000000 ) ) ;
#29718=VERTEX_POINT ( 'NONE', #25831 ) ;
#29734=EDGE_LOOP ( 'NONE', ( #12646, #9462 ) ) ;
#29763=AXIS2_PLACEMENT_3D ( 'NONE', #13646, #32208, #11439 ) ;
#29854=FACE_OUTER_BOUND ( 'NONE', #5273, .T. ) ;
#29876=ADVANCED_FACE ( 'NONE', ( #3141 ), #11313, .T. ) ;
#29985=ORIENTED_EDGE ( 'NONE', *, *, #18552, .T. ) ;
#29998=CARTESIAN_POINT ( 'NONE',  ( 2.000000000000000000, 1.329782007511006725, 0.7677499999999987113 ) ) ;
#30041=DIRECTION ( 'NONE',  ( 0.000000000000000000, 0.000000000000000000, 1.000000000000000000 ) ) ;
#30071=ORIENTED_EDGE ( 'NONE', *, *, #26240, .T. ) ;
#30073=VERTEX_POINT ( 'NONE', #18820 ) ;
#30083=CIRCLE ( 'NONE', #14306, 1.535500000000000087 ) ;
#30102=EDGE_CURVE ( 'NONE', #13858, #22150, #25498, .T. ) ;
#30112=PLANE ( 'NONE',  #26035 ) ;
#30134=PRESENTATION_STYLE_ASSIGNMENT (( #22121 ) ) ;
#30142=CIRCLE ( 'NONE', #5654, 1.535500000000000087 ) ;
#30159=CARTESIAN_POINT ( 'NONE',  ( 2.000000000000000000, 0.8865213383406723713, 1.535499999999998755 ) ) ;
#30160=EDGE_LOOP ( 'NONE', ( #7193, #32786, #2771, #8558, #6079 ) ) ;
#30280=DIRECTION ( 'NONE',  ( -1.000000000000000000, -0.000000000000000000, -0.000000000000000000 ) ) ;
#30289=LINE ( 'NONE', #6955, #9870 ) ;
#30292=ADVANCED_FACE ( 'NONE', ( #27616 ), #14676, .T. ) ;
#30335=DIRECTION ( 'NONE',  ( -1.000000000000000000, -0.000000000000000000, -0.000000000000000000 ) ) ;
#30402=ADVANCED_FACE ( 'NONE', ( #26412 ), #10428, .F. ) ;
#30416=VERTEX_POINT ( 'NONE', #20800 ) ;
#30421=AXIS2_PLACEMENT_3D ( 'NONE', #12973, #2415, #10919 ) ;
#30422=PLANE ( 'NONE',  #5875 ) ;
#30433=FACE_OUTER_BOUND ( 'NONE', #19925, .T. ) ;
#30457=CARTESIAN_POINT ( 'NONE',  ( 4.000000000000001776, 2.694222958124178486E-16, 2.200000000000001066 ) ) ;
#30527=CARTESIAN_POINT ( 'NONE',  ( 4.000000000000003553, 0.000000000000000000, 0.000000000000000000 ) ) ;
#30531=ORIENTED_EDGE ( 'NONE', *, *, #21202, .F. ) ;
#30539=FACE_OUTER_BOUND ( 'NONE', #26921, .T. ) ;
#30555=CARTESIAN_POINT ( 'NONE',  ( 2.000000000000000000, 1.773042676681340968, -2.276824562219559311E-15 ) ) ;
#30623=VECTOR ( 'NONE', #1279, 1000.000000000000000 ) ;
#30650=CIRCLE ( 'NONE', #19205, 1.535500000000000087 ) ;
#30751=LINE ( 'NONE', #9454, #10524 ) ;
#30765=CARTESIAN_POINT ( 'NONE',  ( -31.74999999999995737, 0.000000000000000000, 2.000000000000000888 ) ) ;
#30837=ADVANCED_FACE ( 'NONE', ( #22545 ), #24766, .T. ) ;
#30844=CARTESIAN_POINT ( 'NONE',  ( 4.000000000000000000, 3.500000000000000000, 0.000000000000000000 ) ) ;
#30915=CARTESIAN_POINT ( 'NONE',  ( 4.200000000000001954, 0.000000000000000000, 2.000000000000000888 ) ) ;
#30920=DIRECTION ( 'NONE',  ( -1.000000000000000000, -0.000000000000000000, -0.000000000000000000 ) ) ;
#30963=AXIS2_PLACEMENT_3D ( 'NONE', #26326, #16263, #5866 ) ;
#31003=ORIENTED_EDGE ( 'NONE', *, *, #31847, .F. ) ;
#31083=LINE ( 'NONE', #23409, #11566 ) ;
#31195=CARTESIAN_POINT ( 'NONE',  ( 2.000000000000000000, 0.8865213383406723713, 1.535499999999998755 ) ) ;
#31219=VERTEX_POINT ( 'NONE', #3722 ) ;
#31221=ADVANCED_FACE ( 'NONE', ( #28833 ), #16833, .F. ) ;
#31224=ORIENTED_EDGE ( 'NONE', *, *, #12220, .F. ) ;
#31236=LINE ( 'NONE', #15883, #17065 ) ;
#31254=EDGE_LOOP ( 'NONE', ( #6001, #20409, #7754 ) ) ;
#31309=( NAMED_UNIT ( * ) PLANE_ANGLE_UNIT ( ) SI_UNIT ( $, .RADIAN. ) );
#31410=DIRECTION ( 'NONE',  ( 0.000000000000000000, -1.224646799147353207E-16, 1.000000000000000000 ) ) ;
#31415=LINE ( 'NONE', #8084, #31685 ) ;
#31430=DIRECTION ( 'NONE',  ( 0.000000000000000000, 0.000000000000000000, 1.000000000000000000 ) ) ;
#31437=AXIS2_PLACEMENT_3D ( 'NONE', #4479, #19651, #30041 ) ;
#31606=EDGE_CURVE ( 'NONE', #9623, #15658, #16660, .T. ) ;
#31685=VECTOR ( 'NONE', #2801, 1000.000000000000227 ) ;
#31692=ORIENTED_EDGE ( 'NONE', *, *, #25545, .T. ) ;
#31750=VECTOR ( 'NONE', #27809, 1000.000000000000227 ) ;
#31847=EDGE_CURVE ( 'NONE', #8400, #9623, #23302, .T. ) ;
#31853=EDGE_LOOP ( 'NONE', ( #3499, #7718, #15195, #17798, #8947 ) ) ;
#31905=ORIENTED_EDGE ( 'NONE', *, *, #7291, .T. ) ;
#31980=EDGE_CURVE ( 'NONE', #4155, #6185, #28475, .T. ) ;
#32024=ORIENTED_EDGE ( 'NONE', *, *, #33659, .T. ) ;
#32062=EDGE_CURVE ( 'NONE', #10890, #25762, #30083, .T. ) ;
#32075=AXIS2_PLACEMENT_3D ( 'NONE', #19955, #14502, #32227 ) ;
#32112=VERTEX_POINT ( 'NONE', #13621 ) ;
#32208=DIRECTION ( 'NONE',  ( -1.000000000000000000, -0.000000000000000000, -0.000000000000000000 ) ) ;
#32227=DIRECTION ( 'NONE',  ( 0.000000000000000000, 0.000000000000000000, 1.000000000000000000 ) ) ;
#32446=ORIENTED_EDGE ( 'NONE', *, *, #15827, .T. ) ;
#32660=CARTESIAN_POINT ( 'NONE',  ( 2.000000000000000000, 1.773042676681340968, -2.276824562219559311E-15 ) ) ;
#32786=ORIENTED_EDGE ( 'NONE', *, *, #17216, .F. ) ;
#32836=ORIENTED_EDGE ( 'NONE', *, *, #1631, .F. ) ;
#32858=AXIS2_PLACEMENT_3D ( 'NONE', #8255, #18644, #5852 ) ;
#32889=ADVANCED_FACE ( 'NONE', ( #15483 ), #28266, .F. ) ;
#32904=CARTESIAN_POINT ( 'NONE',  ( -31.74999999999995737, 0.000000000000000000, 0.000000000000000000 ) ) ;
#32920=DIRECTION ( 'NONE',  ( -1.000000000000000000, 0.000000000000000000, -0.000000000000000000 ) ) ;
#32959=ORIENTED_EDGE ( 'NONE', *, *, #22246, .T. ) ;
#33042=EDGE_CURVE ( 'NONE', #6483, #16822, #6725, .T. ) ;
#33126=TOROIDAL_SURFACE ( 'NONE', #11385, 2.200000000000001066, 0.2000000000000000111 ) ;
#33144=DIRECTION ( 'NONE',  ( 0.000000000000000000, 1.000000000000000000, -1.100686371591861952E-15 ) ) ;
#33212=AXIS2_PLACEMENT_3D ( 'NONE', #1012, #11407, #8352 ) ;
#33222=ADVANCED_FACE ( 'NONE', ( #12695 ), #2814, .T. ) ;
#33252=FACE_OUTER_BOUND ( 'NONE', #27145, .T. ) ;
#33256=EDGE_CURVE ( 'NONE', #32112, #16822, #28548, .T. ) ;
#33268=DIRECTION ( 'NONE',  ( 0.000000000000000000, 0.000000000000000000, 1.000000000000000000 ) ) ;
#33309=LINE ( 'NONE', #28200, #9635 ) ;
#33322=CARTESIAN_POINT ( 'NONE',  ( 16.00000000000000000, 0.000000000000000000, 1.610000000000000098 ) ) ;
#33340=ORIENTED_EDGE ( 'NONE', *, *, #24518, .F. ) ;
#33344=EDGE_LOOP ( 'NONE', ( #10962, #23738, #26838, #30531 ) ) ;
#33455=ORIENTED_EDGE ( 'NONE', *, *, #12220, .T. ) ;
#33475=DIRECTION ( 'NONE',  ( 1.000000000000000000, 0.000000000000000000, 0.000000000000000000 ) ) ;
#33481=DIRECTION ( 'NONE',  ( -1.000000000000000000, -0.000000000000000000, -0.000000000000000000 ) ) ;
#33519=AXIS2_PLACEMENT_3D ( 'NONE', #24993, #17658, #17822 ) ;
#33561=PLANE ( 'NONE',  #5808 ) ;
#33592=CARTESIAN_POINT ( 'NONE',  ( 0.1999999999999987899, 0.000000000000000000, 0.000000000000000000 ) ) ;
#33659=EDGE_CURVE ( 'NONE', #14984, #2476, #30142, .T. ) ;
#33678=ORIENTED_EDGE ( 'NONE', *, *, #25603, .T. ) ;
ENDSEC;
END-ISO-10303-21;
